ISO-10303-21;
HEADER;
/* Generated by software containing ST-Developer
 * from STEP Tools, Inc. (www.steptools.com) 
 */

FILE_DESCRIPTION(
/* description */ (''),
/* implementation_level */ '2;1');

FILE_NAME(
/* name */ 'Disc_01.step',
/* time_stamp */ '2026-10-04T16:36:43-07:00',
/* author */ (''),
/* organization */ (''),
/* preprocessor_version */ 'ST-DEVELOPER v20.2',
/* originating_system */ 'Autodesk Translation Framework v15.15.0.0',
/* authorisation */ '');

FILE_SCHEMA (('AUTOMOTIVE_DESIGN { 1 0 10303 214 3 1 1 }'));
ENDSEC;

DATA;
#10=MECHANICAL_DESIGN_GEOMETRIC_PRESENTATION_REPRESENTATION('',(#68),#33474);
#31=(
BOUNDED_CURVE()
B_SPLINE_CURVE(5,(#31814,#31815,#31816,#31817,#31818,#31819,#31820,#31821,
#31822,#31823,#31824,#31825,#31826,#31827,#31828,#31829,#31830,#31831,#31832,
#31833,#31834,#31835,#31836,#31837,#31838),.UNSPECIFIED.,.F.,.F.)
B_SPLINE_CURVE_WITH_KNOTS((6,5,1,1,1,1,1,1,1,1,1,1,1,1,1,1,6),(-0.120132019601874,
0.,0.0666666666666667,0.133333333333333,0.2,0.266666666666667,0.333333333333333,
0.4,0.466666666666667,0.533333333333333,0.6,0.666666666666667,0.733333333333333,
0.8,0.866666666666667,0.933333333333333,1.),.UNSPECIFIED.)
CURVE()
GEOMETRIC_REPRESENTATION_ITEM()
RATIONAL_B_SPLINE_CURVE((1.,1.,1.,1.,1.,1.,1.,1.,1.,1.,1.,1.,1.,1.,1.,1.,
1.,1.,1.,1.,1.,1.,1.,1.,1.))
REPRESENTATION_ITEM('')
);
#47=(
BOUNDED_SURFACE()
B_SPLINE_SURFACE(5,2,((#31588,#31589,#31590,#31591,#31592,#31593,#31594,
#31595,#31596),(#31597,#31598,#31599,#31600,#31601,#31602,#31603,#31604,
#31605),(#31606,#31607,#31608,#31609,#31610,#31611,#31612,#31613,#31614),
(#31615,#31616,#31617,#31618,#31619,#31620,#31621,#31622,#31623),(#31624,
#31625,#31626,#31627,#31628,#31629,#31630,#31631,#31632),(#31633,#31634,
#31635,#31636,#31637,#31638,#31639,#31640,#31641),(#31642,#31643,#31644,
#31645,#31646,#31647,#31648,#31649,#31650),(#31651,#31652,#31653,#31654,
#31655,#31656,#31657,#31658,#31659),(#31660,#31661,#31662,#31663,#31664,
#31665,#31666,#31667,#31668),(#31669,#31670,#31671,#31672,#31673,#31674,
#31675,#31676,#31677),(#31678,#31679,#31680,#31681,#31682,#31683,#31684,
#31685,#31686),(#31687,#31688,#31689,#31690,#31691,#31692,#31693,#31694,
#31695),(#31696,#31697,#31698,#31699,#31700,#31701,#31702,#31703,#31704),
(#31705,#31706,#31707,#31708,#31709,#31710,#31711,#31712,#31713),(#31714,
#31715,#31716,#31717,#31718,#31719,#31720,#31721,#31722),(#31723,#31724,
#31725,#31726,#31727,#31728,#31729,#31730,#31731),(#31732,#31733,#31734,
#31735,#31736,#31737,#31738,#31739,#31740),(#31741,#31742,#31743,#31744,
#31745,#31746,#31747,#31748,#31749),(#31750,#31751,#31752,#31753,#31754,
#31755,#31756,#31757,#31758),(#31759,#31760,#31761,#31762,#31763,#31764,
#31765,#31766,#31767),(#31768,#31769,#31770,#31771,#31772,#31773,#31774,
#31775,#31776),(#31777,#31778,#31779,#31780,#31781,#31782,#31783,#31784,
#31785),(#31786,#31787,#31788,#31789,#31790,#31791,#31792,#31793,#31794),
(#31795,#31796,#31797,#31798,#31799,#31800,#31801,#31802,#31803),(#31804,
#31805,#31806,#31807,#31808,#31809,#31810,#31811,#31812)),.UNSPECIFIED.,
 .F.,.T.,.F.)
B_SPLINE_SURFACE_WITH_KNOTS((6,5,1,1,1,1,1,1,1,1,1,1,1,1,1,1,6),(3,2,2,
2,3),(-0.300330049004687,0.,0.0666666666666667,0.133333333333333,0.2,0.266666666666667,
0.333333333333333,0.4,0.466666666666667,0.533333333333333,0.6,0.666666666666667,
0.733333333333333,0.8,0.866666666666667,0.933333333333333,1.),(0.,1.5707963267949,
3.14159265358979,4.71238898038469,6.28318530717959),.UNSPECIFIED.)
GEOMETRIC_REPRESENTATION_ITEM()
RATIONAL_B_SPLINE_SURFACE(((1.,0.707106781186548,1.,0.707106781186548,1.,
0.707106781186548,1.,0.707106781186548,1.),(1.,0.707106781186548,1.,0.707106781186548,
1.,0.707106781186548,1.,0.707106781186548,1.),(1.,0.707106781186548,1.,
0.707106781186548,1.,0.707106781186548,1.,0.707106781186548,1.),(1.,0.707106781186548,
1.,0.707106781186548,1.,0.707106781186548,1.,0.707106781186548,1.),(1.,
0.707106781186548,1.,0.707106781186548,1.,0.707106781186548,1.,0.707106781186548,
1.),(1.,0.707106781186548,1.,0.707106781186548,1.,0.707106781186548,1.,
0.707106781186548,1.),(1.,0.707106781186548,1.,0.707106781186548,1.,0.707106781186548,
1.,0.707106781186548,1.),(1.,0.707106781186548,1.,0.707106781186548,1.,
0.707106781186548,1.,0.707106781186548,1.),(1.,0.707106781186548,1.,0.707106781186548,
1.,0.707106781186548,1.,0.707106781186548,1.),(1.,0.707106781186548,1.,
0.707106781186548,1.,0.707106781186548,1.,0.707106781186548,1.),(1.,0.707106781186548,
1.,0.707106781186548,1.,0.707106781186548,1.,0.707106781186548,1.),(1.,
0.707106781186548,1.,0.707106781186548,1.,0.707106781186548,1.,0.707106781186548,
1.),(1.,0.707106781186548,1.,0.707106781186548,1.,0.707106781186548,1.,
0.707106781186548,1.),(1.,0.707106781186548,1.,0.707106781186548,1.,0.707106781186548,
1.,0.707106781186548,1.),(1.,0.707106781186548,1.,0.707106781186548,1.,
0.707106781186548,1.,0.707106781186548,1.),(1.,0.707106781186548,1.,0.707106781186548,
1.,0.707106781186548,1.,0.707106781186548,1.),(1.,0.707106781186548,1.,
0.707106781186548,1.,0.707106781186548,1.,0.707106781186548,1.),(1.,0.707106781186548,
1.,0.707106781186548,1.,0.707106781186548,1.,0.707106781186548,1.),(1.,
0.707106781186548,1.,0.707106781186548,1.,0.707106781186548,1.,0.707106781186548,
1.),(1.,0.707106781186548,1.,0.707106781186548,1.,0.707106781186548,1.,
0.707106781186548,1.),(1.,0.707106781186548,1.,0.707106781186548,1.,0.707106781186548,
1.,0.707106781186548,1.),(1.,0.707106781186548,1.,0.707106781186548,1.,
0.707106781186548,1.,0.707106781186548,1.),(1.,0.707106781186548,1.,0.707106781186548,
1.,0.707106781186548,1.,0.707106781186548,1.),(1.,0.707106781186548,1.,
0.707106781186548,1.,0.707106781186548,1.,0.707106781186548,1.),(1.,0.707106781186548,
1.,0.707106781186548,1.,0.707106781186548,1.,0.707106781186548,1.)))
REPRESENTATION_ITEM('')
SURFACE()
);
#48=(
BOUNDED_SURFACE()
B_SPLINE_SURFACE(3,2,((#31924,#31925,#31926,#31927,#31928,#31929,#31930,
#31931,#31932),(#31933,#31934,#31935,#31936,#31937,#31938,#31939,#31940,
#31941),(#31942,#31943,#31944,#31945,#31946,#31947,#31948,#31949,#31950),
(#31951,#31952,#31953,#31954,#31955,#31956,#31957,#31958,#31959),(#31960,
#31961,#31962,#31963,#31964,#31965,#31966,#31967,#31968),(#31969,#31970,
#31971,#31972,#31973,#31974,#31975,#31976,#31977),(#31978,#31979,#31980,
#31981,#31982,#31983,#31984,#31985,#31986),(#31987,#31988,#31989,#31990,
#31991,#31992,#31993,#31994,#31995),(#31996,#31997,#31998,#31999,#32000,
#32001,#32002,#32003,#32004),(#32005,#32006,#32007,#32008,#32009,#32010,
#32011,#32012,#32013),(#32014,#32015,#32016,#32017,#32018,#32019,#32020,
#32021,#32022),(#32023,#32024,#32025,#32026,#32027,#32028,#32029,#32030,
#32031),(#32032,#32033,#32034,#32035,#32036,#32037,#32038,#32039,#32040)),
 .UNSPECIFIED.,.F.,.T.,.F.)
B_SPLINE_SURFACE_WITH_KNOTS((4,3,3,3,4),(3,2,2,2,3),(-0.984123122879426,
-0.97309206569331,-0.499330519660681,-0.00706539599512239,0.2972933688639),
(0.,1.5707963267949,3.14159265358979,4.71238898038469,6.28318530717959),
 .UNSPECIFIED.)
GEOMETRIC_REPRESENTATION_ITEM()
RATIONAL_B_SPLINE_SURFACE(((1.,0.707106781186548,1.,0.707106781186548,1.,
0.707106781186548,1.,0.707106781186548,1.),(1.,0.707106781186548,1.,0.707106781186548,
1.,0.707106781186548,1.,0.707106781186548,1.),(1.,0.707106781186548,1.,
0.707106781186548,1.,0.707106781186548,1.,0.707106781186548,1.),(1.,0.707106781186548,
1.,0.707106781186548,1.,0.707106781186548,1.,0.707106781186548,1.),(1.,
0.707106781186548,1.,0.707106781186548,1.,0.707106781186548,1.,0.707106781186548,
1.),(1.,0.707106781186548,1.,0.707106781186548,1.,0.707106781186548,1.,
0.707106781186548,1.),(1.,0.707106781186548,1.,0.707106781186548,1.,0.707106781186548,
1.,0.707106781186548,1.),(1.,0.707106781186548,1.,0.707106781186548,1.,
0.707106781186548,1.,0.707106781186548,1.),(1.,0.707106781186548,1.,0.707106781186548,
1.,0.707106781186548,1.,0.707106781186548,1.),(1.,0.707106781186548,1.,
0.707106781186548,1.,0.707106781186548,1.,0.707106781186548,1.),(1.,0.707106781186548,
1.,0.707106781186548,1.,0.707106781186548,1.,0.707106781186548,1.),(1.,
0.707106781186548,1.,0.707106781186548,1.,0.707106781186548,1.,0.707106781186548,
1.),(1.,0.707106781186548,1.,0.707106781186548,1.,0.707106781186548,1.,
0.707106781186548,1.)))
REPRESENTATION_ITEM('')
SURFACE()
);
#51=CONICAL_SURFACE('',#3090,16.067990296595,0.959931088596882);
#52=CONICAL_SURFACE('',#3096,15.7712719335665,0.959931088596882);
#58=SHAPE_REPRESENTATION_RELATIONSHIP('SRR','None',#33498,#63);
#63=ADVANCED_BREP_SHAPE_REPRESENTATION('',(#73),#33470);
#68=STYLED_ITEM('',(#33531),#73);
#73=MANIFOLD_SOLID_BREP('Body1',#2808);
#78=TOROIDAL_SURFACE('',#3093,16.9386060980155,0.25);
#79=TOROIDAL_SURFACE('',#3098,13.4131653526691,1.72390117308562);
#80=TOROIDAL_SURFACE('',#3105,13.4131653526691,2.22390117308562);
#187=LINE('',#31572,#284);
#188=LINE('',#31581,#285);
#189=LINE('',#31923,#286);
#284=VECTOR('',#3679,16.067990296595);
#285=VECTOR('',#3692,15.7712719335665);
#286=VECTOR('',#3703,3.5);
#390=FACE_OUTER_BOUND('',#513,.T.);
#391=FACE_OUTER_BOUND('',#514,.T.);
#392=FACE_OUTER_BOUND('',#515,.T.);
#393=FACE_OUTER_BOUND('',#516,.T.);
#394=FACE_OUTER_BOUND('',#517,.T.);
#395=FACE_OUTER_BOUND('',#518,.T.);
#396=FACE_OUTER_BOUND('',#519,.T.);
#397=FACE_OUTER_BOUND('',#520,.T.);
#513=EDGE_LOOP('',(#2459,#2460,#2461,#2462));
#514=EDGE_LOOP('',(#2463,#2464,#2465,#2466));
#515=EDGE_LOOP('',(#2467,#2468,#2469,#2470));
#516=EDGE_LOOP('',(#2471,#2472,#2473,#2474,#2475));
#517=EDGE_LOOP('',(#2476,#2477,#2478,#2479,#2480,#2481));
#518=EDGE_LOOP('',(#2482,#2483,#2484,#2485,#2486,#2487));
#519=EDGE_LOOP('',(#2488,#2489,#2490,#2491,#2492,#2493));
#520=EDGE_LOOP('',(#2494,#2495,#2496,#2497,#2498));
#675=CIRCLE('',#3091,17.0820002071033);
#676=CIRCLE('',#3092,14.8491923750145);
#677=CIRCLE('',#3094,16.7952119889278);
#678=CIRCLE('',#3095,0.25);
#679=CIRCLE('',#3097,14.542543867133);
#680=CIRCLE('',#3099,12.2837868382051);
#681=CIRCLE('',#3100,12.2837868382051);
#682=CIRCLE('',#3101,1.72390117308562);
#683=CIRCLE('',#3103,12.0671767507335);
#684=CIRCLE('',#3104,12.0671767507335);
#685=CIRCLE('',#3106,2.22390117308562);
#875=B_SPLINE_CURVE_WITH_KNOTS('',3,(#31840,#31841,#31842,#31843,#31844,
#31845,#31846,#31847,#31848,#31849,#31850,#31851,#31852,#31853,#31854,#31855,
#31856,#31857,#31858,#31859),.UNSPECIFIED.,.F.,.F.,(4,2,2,2,2,2,2,2,2,4),
(-0.787824152103525,-0.776665386905323,-0.683544248464441,-0.586951582106689,
-0.487645947294414,-0.388535605921421,-0.295627476504987,-0.199263976847017,
-0.0990296104815163,0.),.UNSPECIFIED.);
#876=B_SPLINE_CURVE_WITH_KNOTS('',3,(#31860,#31861,#31862,#31863,#31864,
#31865,#31866,#31867,#31868,#31869,#31870,#31871,#31872,#31873,#31874,#31875,
#31876,#31877,#31878,#31879),.UNSPECIFIED.,.F.,.F.,(4,2,2,2,2,2,2,2,2,4),
(0.,0.0550500400736549,0.113849056000799,0.210816540693219,0.310109597556883,
0.410211670547243,0.50352797305395,0.600331621930534,0.699630608578638,
0.787671103816309),.UNSPECIFIED.);
#877=B_SPLINE_CURVE_WITH_KNOTS('',3,(#31883,#31884,#31885,#31886,#31887,
#31888,#31889,#31890,#31891,#31892,#31893,#31894,#31895,#31896,#31897,#31898,
#31899,#31900,#31901,#31902),.UNSPECIFIED.,.F.,.F.,(4,2,2,2,2,2,2,2,2,4),
(-0.787824152103524,-0.776665386905322,-0.68354424846444,-0.586951582106688,
-0.487645947294413,-0.388535605921421,-0.295627476504987,-0.199263976847016,
-0.099029610481516,0.),.UNSPECIFIED.);
#878=B_SPLINE_CURVE_WITH_KNOTS('',3,(#31903,#31904,#31905,#31906,#31907,
#31908,#31909,#31910,#31911,#31912,#31913,#31914,#31915,#31916,#31917,#31918,
#31919,#31920,#31921,#31922),.UNSPECIFIED.,.F.,.F.,(4,2,2,2,2,2,2,2,2,4),
(0.,0.0550500400736533,0.113849056000795,0.210816540693215,0.310109597556879,
0.410211670547239,0.503527973053946,0.600331621930529,0.699630608578633,
0.787671103816304),.UNSPECIFIED.);
#879=B_SPLINE_CURVE_WITH_KNOTS('',3,(#32042,#32043,#32044,#32045,#32046,
#32047,#32048,#32049,#32050,#32051,#32052,#32053,#32054),.UNSPECIFIED.,
 .F.,.F.,(4,3,3,3,4),(-0.114678109950221,0.00706539599431312,0.499330519660279,
0.973092065693301,0.984123122879426),.UNSPECIFIED.);
#1187=VERTEX_POINT('',#31569);
#1188=VERTEX_POINT('',#31571);
#1189=VERTEX_POINT('',#31575);
#1190=VERTEX_POINT('',#31579);
#1191=VERTEX_POINT('',#31583);
#1192=VERTEX_POINT('',#31584);
#1193=VERTEX_POINT('',#31813);
#1194=VERTEX_POINT('',#31839);
#1195=VERTEX_POINT('',#31881);
#1196=VERTEX_POINT('',#31882);
#1197=VERTEX_POINT('',#32041);
#1198=VERTEX_POINT('',#32055);
#1617=EDGE_CURVE('',#1187,#1187,#675,.T.);
#1618=EDGE_CURVE('',#1187,#1188,#187,.T.);
#1619=EDGE_CURVE('',#1188,#1188,#676,.T.);
#1620=EDGE_CURVE('',#1189,#1189,#677,.T.);
#1621=EDGE_CURVE('',#1189,#1187,#678,.T.);
#1622=EDGE_CURVE('',#1190,#1190,#679,.T.);
#1623=EDGE_CURVE('',#1190,#1189,#188,.T.);
#1624=EDGE_CURVE('',#1191,#1192,#680,.T.);
#1625=EDGE_CURVE('',#1192,#1191,#681,.T.);
#1626=EDGE_CURVE('',#1192,#1190,#682,.T.);
#1627=EDGE_CURVE('',#1193,#1191,#31,.T.);
#1628=EDGE_CURVE('',#1194,#1193,#875,.F.);
#1629=EDGE_CURVE('',#1193,#1194,#876,.F.);
#1630=EDGE_CURVE('',#1195,#1196,#877,.T.);
#1631=EDGE_CURVE('',#1196,#1195,#878,.T.);
#1632=EDGE_CURVE('',#1196,#1194,#189,.T.);
#1633=EDGE_CURVE('',#1195,#1197,#879,.T.);
#1634=EDGE_CURVE('',#1198,#1197,#683,.T.);
#1635=EDGE_CURVE('',#1197,#1198,#684,.T.);
#1636=EDGE_CURVE('',#1188,#1198,#685,.T.);
#2459=ORIENTED_EDGE('',*,*,#1617,.F.);
#2460=ORIENTED_EDGE('',*,*,#1618,.T.);
#2461=ORIENTED_EDGE('',*,*,#1619,.T.);
#2462=ORIENTED_EDGE('',*,*,#1618,.F.);
#2463=ORIENTED_EDGE('',*,*,#1620,.T.);
#2464=ORIENTED_EDGE('',*,*,#1621,.T.);
#2465=ORIENTED_EDGE('',*,*,#1617,.T.);
#2466=ORIENTED_EDGE('',*,*,#1621,.F.);
#2467=ORIENTED_EDGE('',*,*,#1622,.F.);
#2468=ORIENTED_EDGE('',*,*,#1623,.T.);
#2469=ORIENTED_EDGE('',*,*,#1620,.F.);
#2470=ORIENTED_EDGE('',*,*,#1623,.F.);
#2471=ORIENTED_EDGE('',*,*,#1624,.F.);
#2472=ORIENTED_EDGE('',*,*,#1625,.F.);
#2473=ORIENTED_EDGE('',*,*,#1626,.T.);
#2474=ORIENTED_EDGE('',*,*,#1622,.T.);
#2475=ORIENTED_EDGE('',*,*,#1626,.F.);
#2476=ORIENTED_EDGE('',*,*,#1627,.T.);
#2477=ORIENTED_EDGE('',*,*,#1624,.T.);
#2478=ORIENTED_EDGE('',*,*,#1625,.T.);
#2479=ORIENTED_EDGE('',*,*,#1627,.F.);
#2480=ORIENTED_EDGE('',*,*,#1628,.F.);
#2481=ORIENTED_EDGE('',*,*,#1629,.F.);
#2482=ORIENTED_EDGE('',*,*,#1630,.F.);
#2483=ORIENTED_EDGE('',*,*,#1631,.F.);
#2484=ORIENTED_EDGE('',*,*,#1632,.T.);
#2485=ORIENTED_EDGE('',*,*,#1628,.T.);
#2486=ORIENTED_EDGE('',*,*,#1629,.T.);
#2487=ORIENTED_EDGE('',*,*,#1632,.F.);
#2488=ORIENTED_EDGE('',*,*,#1633,.F.);
#2489=ORIENTED_EDGE('',*,*,#1630,.T.);
#2490=ORIENTED_EDGE('',*,*,#1631,.T.);
#2491=ORIENTED_EDGE('',*,*,#1633,.T.);
#2492=ORIENTED_EDGE('',*,*,#1634,.F.);
#2493=ORIENTED_EDGE('',*,*,#1635,.F.);
#2494=ORIENTED_EDGE('',*,*,#1619,.F.);
#2495=ORIENTED_EDGE('',*,*,#1636,.T.);
#2496=ORIENTED_EDGE('',*,*,#1634,.T.);
#2497=ORIENTED_EDGE('',*,*,#1635,.T.);
#2498=ORIENTED_EDGE('',*,*,#1636,.F.);
#2683=CYLINDRICAL_SURFACE('',#3102,2.5);
#2777=ADVANCED_FACE('',(#390),#51,.T.);
#2778=ADVANCED_FACE('',(#391),#78,.T.);
#2779=ADVANCED_FACE('',(#392),#52,.F.);
#2780=ADVANCED_FACE('',(#393),#79,.F.);
#2781=ADVANCED_FACE('',(#394),#47,.T.);
#2782=ADVANCED_FACE('',(#395),#2683,.F.);
#2783=ADVANCED_FACE('',(#396),#48,.T.);
#2784=ADVANCED_FACE('',(#397),#80,.T.);
#2808=CLOSED_SHELL('',(#2777,#2778,#2779,#2780,#2781,#2782,#2783,#2784));
#3089=AXIS2_PLACEMENT_3D('',#31567,#3673,#3674);
#3090=AXIS2_PLACEMENT_3D('',#31568,#3675,#3676);
#3091=AXIS2_PLACEMENT_3D('',#31570,#3677,#3678);
#3092=AXIS2_PLACEMENT_3D('',#31573,#3680,#3681);
#3093=AXIS2_PLACEMENT_3D('',#31574,#3682,#3683);
#3094=AXIS2_PLACEMENT_3D('',#31576,#3684,#3685);
#3095=AXIS2_PLACEMENT_3D('',#31577,#3686,#3687);
#3096=AXIS2_PLACEMENT_3D('',#31578,#3688,#3689);
#3097=AXIS2_PLACEMENT_3D('',#31580,#3690,#3691);
#3098=AXIS2_PLACEMENT_3D('',#31582,#3693,#3694);
#3099=AXIS2_PLACEMENT_3D('',#31585,#3695,#3696);
#3100=AXIS2_PLACEMENT_3D('',#31586,#3697,#3698);
#3101=AXIS2_PLACEMENT_3D('',#31587,#3699,#3700);
#3102=AXIS2_PLACEMENT_3D('',#31880,#3701,#3702);
#3103=AXIS2_PLACEMENT_3D('',#32056,#3704,#3705);
#3104=AXIS2_PLACEMENT_3D('',#32057,#3706,#3707);
#3105=AXIS2_PLACEMENT_3D('',#32058,#3708,#3709);
#3106=AXIS2_PLACEMENT_3D('',#32059,#3710,#3711);
#3673=DIRECTION('axis',(0.,0.,1.));
#3674=DIRECTION('refdir',(1.,0.,0.));
#3675=DIRECTION('center_axis',(0.,0.,1.));
#3676=DIRECTION('ref_axis',(1.,0.,0.));
#3677=DIRECTION('center_axis',(0.,0.,1.));
#3678=DIRECTION('ref_axis',(-1.,0.,0.));
#3679=DIRECTION('',(0.819152044288992,1.00317192905353E-16,-0.573576436351045));
#3680=DIRECTION('center_axis',(0.,0.,1.));
#3681=DIRECTION('ref_axis',(1.,0.,0.));
#3682=DIRECTION('center_axis',(0.,0.,1.));
#3683=DIRECTION('ref_axis',(1.,0.,0.));
#3684=DIRECTION('center_axis',(0.,0.,-1.));
#3685=DIRECTION('ref_axis',(-1.,0.,0.));
#3686=DIRECTION('center_axis',(1.22464679914735E-16,-1.,0.));
#3687=DIRECTION('ref_axis',(-1.,-1.22464679914735E-16,0.));
#3688=DIRECTION('center_axis',(0.,0.,1.));
#3689=DIRECTION('ref_axis',(1.,0.,0.));
#3690=DIRECTION('center_axis',(0.,0.,1.));
#3691=DIRECTION('ref_axis',(1.,0.,0.));
#3692=DIRECTION('',(-0.819152044288992,-1.00317192905353E-16,0.573576436351045));
#3693=DIRECTION('center_axis',(0.,0.,1.));
#3694=DIRECTION('ref_axis',(1.,0.,0.));
#3695=DIRECTION('center_axis',(0.,0.,1.));
#3696=DIRECTION('ref_axis',(1.,0.,0.));
#3697=DIRECTION('center_axis',(0.,0.,1.));
#3698=DIRECTION('ref_axis',(1.,0.,0.));
#3699=DIRECTION('center_axis',(-1.22464679914735E-16,1.,0.));
#3700=DIRECTION('ref_axis',(-1.,-1.22464679914735E-16,0.));
#3701=DIRECTION('center_axis',(0.,0.,1.));
#3702=DIRECTION('ref_axis',(1.,0.,0.));
#3703=DIRECTION('',(0.,0.,1.));
#3704=DIRECTION('center_axis',(0.,0.,1.));
#3705=DIRECTION('ref_axis',(1.,0.,0.));
#3706=DIRECTION('center_axis',(0.,0.,1.));
#3707=DIRECTION('ref_axis',(1.,0.,0.));
#3708=DIRECTION('center_axis',(0.,0.,1.));
#3709=DIRECTION('ref_axis',(1.,0.,0.));
#3710=DIRECTION('center_axis',(1.22464679914735E-16,-1.,0.));
#3711=DIRECTION('ref_axis',(-1.,-1.22464679914735E-16,0.));
#31567=CARTESIAN_POINT('',(0.,0.,0.));
#31568=CARTESIAN_POINT('Origin',(0.,0.,25.1187110682415));
#31569=CARTESIAN_POINT('',(-17.0820002071033,-2.09194168766635E-15,25.8287284513987));
#31570=CARTESIAN_POINT('Origin',(0.,-2.09194168766635E-15,25.8287284513987));
#31571=CARTESIAN_POINT('',(-14.8491923750145,-1.81850159119848E-15,24.2652995759965));
#31572=CARTESIAN_POINT('',(-16.067990296595,-1.96776128854558E-15,25.1187110682415));
#31573=CARTESIAN_POINT('Origin',(0.,0.,24.2652995759965));
#31574=CARTESIAN_POINT('Origin',(0.,0.,26.033516462471));
#31575=CARTESIAN_POINT('',(-16.7952119889278,-2.05682026032416E-15,26.2383044735432));
#31576=CARTESIAN_POINT('Origin',(0.,-2.05682026032416E-15,26.2383044735432));
#31577=CARTESIAN_POINT('Origin',(-16.9386060980155,-2.07438097399525E-15,
26.033516462471));
#31578=CARTESIAN_POINT('Origin',(0.,0.,25.5213339281044));
#31579=CARTESIAN_POINT('',(-14.542543867133,-1.78094797983444E-15,24.6609692735778));
#31580=CARTESIAN_POINT('Origin',(0.,0.,24.6609692735778));
#31581=CARTESIAN_POINT('',(-15.7712719335665,-1.93142376919247E-15,25.5213339281044));
#31582=CARTESIAN_POINT('Origin',(0.,0.,25.9634052319394));
#31583=CARTESIAN_POINT('',(12.2837868382051,0.,24.6609692735778));
#31584=CARTESIAN_POINT('',(-12.2837868382051,-1.50433002328163E-15,24.6609692735778));
#31585=CARTESIAN_POINT('Origin',(0.,0.,24.6609692735778));
#31586=CARTESIAN_POINT('Origin',(0.,0.,24.6609692735778));
#31587=CARTESIAN_POINT('Origin',(-13.4131653526691,-1.64263900155804E-15,
25.9634052319394));
#31588=CARTESIAN_POINT('Ctrl Pts',(0.999999999999995,0.,26.6733182859787));
#31589=CARTESIAN_POINT('Ctrl Pts',(0.999999999999995,0.999999999999995,
26.6733182859787));
#31590=CARTESIAN_POINT('Ctrl Pts',(0.,0.999999999999995,26.6733182859787));
#31591=CARTESIAN_POINT('Ctrl Pts',(-0.999999999999995,0.999999999999995,
26.6733182859787));
#31592=CARTESIAN_POINT('Ctrl Pts',(-0.999999999999995,0.,26.6733182859787));
#31593=CARTESIAN_POINT('Ctrl Pts',(-0.999999999999995,-0.999999999999995,
26.6733182859787));
#31594=CARTESIAN_POINT('Ctrl Pts',(0.,-0.999999999999995,26.6733182859787));
#31595=CARTESIAN_POINT('Ctrl Pts',(0.999999999999995,-0.999999999999995,
26.6733182859787));
#31596=CARTESIAN_POINT('Ctrl Pts',(0.999999999999995,0.,26.6733182859787));
#31597=CARTESIAN_POINT('Ctrl Pts',(1.5,0.,26.6149943453092));
#31598=CARTESIAN_POINT('Ctrl Pts',(1.5,1.5,26.6149943453092));
#31599=CARTESIAN_POINT('Ctrl Pts',(0.,1.5,26.6149943453092));
#31600=CARTESIAN_POINT('Ctrl Pts',(-1.5,1.5,26.6149943453092));
#31601=CARTESIAN_POINT('Ctrl Pts',(-1.5,0.,26.6149943453092));
#31602=CARTESIAN_POINT('Ctrl Pts',(-1.5,-1.5,26.6149943453092));
#31603=CARTESIAN_POINT('Ctrl Pts',(0.,-1.5,26.6149943453092));
#31604=CARTESIAN_POINT('Ctrl Pts',(1.5,-1.5,26.6149943453092));
#31605=CARTESIAN_POINT('Ctrl Pts',(1.5,0.,26.6149943453092));
#31606=CARTESIAN_POINT('Ctrl Pts',(2.,0.,26.5566704046396));
#31607=CARTESIAN_POINT('Ctrl Pts',(2.,2.,26.5566704046396));
#31608=CARTESIAN_POINT('Ctrl Pts',(0.,2.,26.5566704046396));
#31609=CARTESIAN_POINT('Ctrl Pts',(-2.,2.,26.5566704046396));
#31610=CARTESIAN_POINT('Ctrl Pts',(-2.,0.,26.5566704046396));
#31611=CARTESIAN_POINT('Ctrl Pts',(-2.,-2.,26.5566704046396));
#31612=CARTESIAN_POINT('Ctrl Pts',(0.,-2.,26.5566704046396));
#31613=CARTESIAN_POINT('Ctrl Pts',(2.,-2.,26.5566704046396));
#31614=CARTESIAN_POINT('Ctrl Pts',(2.,0.,26.5566704046396));
#31615=CARTESIAN_POINT('Ctrl Pts',(2.5,0.,26.4983464639701));
#31616=CARTESIAN_POINT('Ctrl Pts',(2.5,2.5,26.4983464639701));
#31617=CARTESIAN_POINT('Ctrl Pts',(0.,2.5,26.4983464639701));
#31618=CARTESIAN_POINT('Ctrl Pts',(-2.5,2.5,26.4983464639701));
#31619=CARTESIAN_POINT('Ctrl Pts',(-2.5,0.,26.4983464639701));
#31620=CARTESIAN_POINT('Ctrl Pts',(-2.5,-2.5,26.4983464639701));
#31621=CARTESIAN_POINT('Ctrl Pts',(0.,-2.5,26.4983464639701));
#31622=CARTESIAN_POINT('Ctrl Pts',(2.5,-2.5,26.4983464639701));
#31623=CARTESIAN_POINT('Ctrl Pts',(2.5,0.,26.4983464639701));
#31624=CARTESIAN_POINT('Ctrl Pts',(3.,0.,26.4400225233005));
#31625=CARTESIAN_POINT('Ctrl Pts',(3.,3.,26.4400225233005));
#31626=CARTESIAN_POINT('Ctrl Pts',(0.,3.,26.4400225233005));
#31627=CARTESIAN_POINT('Ctrl Pts',(-3.,3.,26.4400225233005));
#31628=CARTESIAN_POINT('Ctrl Pts',(-3.,0.,26.4400225233005));
#31629=CARTESIAN_POINT('Ctrl Pts',(-3.,-3.,26.4400225233005));
#31630=CARTESIAN_POINT('Ctrl Pts',(0.,-3.,26.4400225233005));
#31631=CARTESIAN_POINT('Ctrl Pts',(3.,-3.,26.4400225233005));
#31632=CARTESIAN_POINT('Ctrl Pts',(3.,0.,26.4400225233005));
#31633=CARTESIAN_POINT('Ctrl Pts',(3.5,0.,26.381698582631));
#31634=CARTESIAN_POINT('Ctrl Pts',(3.5,3.5,26.381698582631));
#31635=CARTESIAN_POINT('Ctrl Pts',(0.,3.5,26.381698582631));
#31636=CARTESIAN_POINT('Ctrl Pts',(-3.5,3.5,26.381698582631));
#31637=CARTESIAN_POINT('Ctrl Pts',(-3.5,0.,26.381698582631));
#31638=CARTESIAN_POINT('Ctrl Pts',(-3.5,-3.5,26.381698582631));
#31639=CARTESIAN_POINT('Ctrl Pts',(0.,-3.5,26.381698582631));
#31640=CARTESIAN_POINT('Ctrl Pts',(3.5,-3.5,26.381698582631));
#31641=CARTESIAN_POINT('Ctrl Pts',(3.5,0.,26.381698582631));
#31642=CARTESIAN_POINT('Ctrl Pts',(3.61098900507559,0.,26.368751950337));
#31643=CARTESIAN_POINT('Ctrl Pts',(3.61098900507559,3.61098900507559,26.368751950337));
#31644=CARTESIAN_POINT('Ctrl Pts',(0.,3.61098900507559,26.368751950337));
#31645=CARTESIAN_POINT('Ctrl Pts',(-3.61098900507559,3.61098900507559,26.368751950337));
#31646=CARTESIAN_POINT('Ctrl Pts',(-3.61098900507559,0.,26.368751950337));
#31647=CARTESIAN_POINT('Ctrl Pts',(-3.61098900507559,-3.61098900507559,
26.368751950337));
#31648=CARTESIAN_POINT('Ctrl Pts',(0.,-3.61098900507559,26.368751950337));
#31649=CARTESIAN_POINT('Ctrl Pts',(3.61098900507559,-3.61098900507559,26.368751950337));
#31650=CARTESIAN_POINT('Ctrl Pts',(3.61098900507559,0.,26.368751950337));
#31651=CARTESIAN_POINT('Ctrl Pts',(3.83416205501541,0.,26.3417018678852));
#31652=CARTESIAN_POINT('Ctrl Pts',(3.83416205501541,3.83416205501541,26.3417018678852));
#31653=CARTESIAN_POINT('Ctrl Pts',(0.,3.83416205501541,26.3417018678852));
#31654=CARTESIAN_POINT('Ctrl Pts',(-3.83416205501541,3.83416205501541,26.3417018678852));
#31655=CARTESIAN_POINT('Ctrl Pts',(-3.83416205501541,0.,26.3417018678852));
#31656=CARTESIAN_POINT('Ctrl Pts',(-3.83416205501541,-3.83416205501541,
26.3417018678852));
#31657=CARTESIAN_POINT('Ctrl Pts',(0.,-3.83416205501541,26.3417018678852));
#31658=CARTESIAN_POINT('Ctrl Pts',(3.83416205501541,-3.83416205501541,26.3417018678852));
#31659=CARTESIAN_POINT('Ctrl Pts',(3.83416205501541,0.,26.3417018678852));
#31660=CARTESIAN_POINT('Ctrl Pts',(4.17250673641263,0.,26.2976563050266));
#31661=CARTESIAN_POINT('Ctrl Pts',(4.17250673641263,4.17250673641263,26.2976563050266));
#31662=CARTESIAN_POINT('Ctrl Pts',(0.,4.17250673641263,26.2976563050266));
#31663=CARTESIAN_POINT('Ctrl Pts',(-4.17250673641263,4.17250673641263,26.2976563050266));
#31664=CARTESIAN_POINT('Ctrl Pts',(-4.17250673641263,0.,26.2976563050266));
#31665=CARTESIAN_POINT('Ctrl Pts',(-4.17250673641263,-4.17250673641263,
26.2976563050266));
#31666=CARTESIAN_POINT('Ctrl Pts',(0.,-4.17250673641263,26.2976563050266));
#31667=CARTESIAN_POINT('Ctrl Pts',(4.17250673641263,-4.17250673641263,26.2976563050266));
#31668=CARTESIAN_POINT('Ctrl Pts',(4.17250673641263,0.,26.2976563050266));
#31669=CARTESIAN_POINT('Ctrl Pts',(4.63085543889697,0.,26.2319374216757));
#31670=CARTESIAN_POINT('Ctrl Pts',(4.63085543889697,4.63085543889697,26.2319374216757));
#31671=CARTESIAN_POINT('Ctrl Pts',(0.,4.63085543889697,26.2319374216757));
#31672=CARTESIAN_POINT('Ctrl Pts',(-4.63085543889697,4.63085543889697,26.2319374216757));
#31673=CARTESIAN_POINT('Ctrl Pts',(-4.63085543889697,0.,26.2319374216757));
#31674=CARTESIAN_POINT('Ctrl Pts',(-4.63085543889697,-4.63085543889697,
26.2319374216757));
#31675=CARTESIAN_POINT('Ctrl Pts',(0.,-4.63085543889697,26.2319374216757));
#31676=CARTESIAN_POINT('Ctrl Pts',(4.63085543889697,-4.63085543889697,26.2319374216757));
#31677=CARTESIAN_POINT('Ctrl Pts',(4.63085543889697,0.,26.2319374216757));
#31678=CARTESIAN_POINT('Ctrl Pts',(5.21591518523417,0.,26.137974806988));
#31679=CARTESIAN_POINT('Ctrl Pts',(5.21591518523417,5.21591518523417,26.137974806988));
#31680=CARTESIAN_POINT('Ctrl Pts',(0.,5.21591518523417,26.137974806988));
#31681=CARTESIAN_POINT('Ctrl Pts',(-5.21591518523417,5.21591518523417,26.137974806988));
#31682=CARTESIAN_POINT('Ctrl Pts',(-5.21591518523417,0.,26.137974806988));
#31683=CARTESIAN_POINT('Ctrl Pts',(-5.21591518523417,-5.21591518523417,
26.137974806988));
#31684=CARTESIAN_POINT('Ctrl Pts',(0.,-5.21591518523417,26.137974806988));
#31685=CARTESIAN_POINT('Ctrl Pts',(5.21591518523417,-5.21591518523417,26.137974806988));
#31686=CARTESIAN_POINT('Ctrl Pts',(5.21591518523417,0.,26.137974806988));
#31687=CARTESIAN_POINT('Ctrl Pts',(5.81280340273043,0.,26.0322484636216));
#31688=CARTESIAN_POINT('Ctrl Pts',(5.81280340273043,5.81280340273043,26.0322484636216));
#31689=CARTESIAN_POINT('Ctrl Pts',(0.,5.81280340273043,26.0322484636216));
#31690=CARTESIAN_POINT('Ctrl Pts',(-5.81280340273043,5.81280340273043,26.0322484636216));
#31691=CARTESIAN_POINT('Ctrl Pts',(-5.81280340273043,0.,26.0322484636216));
#31692=CARTESIAN_POINT('Ctrl Pts',(-5.81280340273043,-5.81280340273043,
26.0322484636216));
#31693=CARTESIAN_POINT('Ctrl Pts',(0.,-5.81280340273043,26.0322484636216));
#31694=CARTESIAN_POINT('Ctrl Pts',(5.81280340273043,-5.81280340273043,26.0322484636216));
#31695=CARTESIAN_POINT('Ctrl Pts',(5.81280340273043,0.,26.0322484636216));
#31696=CARTESIAN_POINT('Ctrl Pts',(6.42047090449388,0.,25.9152983846727));
#31697=CARTESIAN_POINT('Ctrl Pts',(6.42047090449387,6.42047090449387,25.9152983846727));
#31698=CARTESIAN_POINT('Ctrl Pts',(0.,6.42047090449388,25.9152983846727));
#31699=CARTESIAN_POINT('Ctrl Pts',(-6.42047090449387,6.42047090449387,25.9152983846727));
#31700=CARTESIAN_POINT('Ctrl Pts',(-6.42047090449388,0.,25.9152983846727));
#31701=CARTESIAN_POINT('Ctrl Pts',(-6.42047090449387,-6.42047090449387,
25.9152983846727));
#31702=CARTESIAN_POINT('Ctrl Pts',(0.,-6.42047090449388,25.9152983846727));
#31703=CARTESIAN_POINT('Ctrl Pts',(6.42047090449387,-6.42047090449387,25.9152983846727));
#31704=CARTESIAN_POINT('Ctrl Pts',(6.42047090449388,0.,25.9152983846727));
#31705=CARTESIAN_POINT('Ctrl Pts',(7.0366882084607,0.,25.7884785969494));
#31706=CARTESIAN_POINT('Ctrl Pts',(7.0366882084607,7.0366882084607,25.7884785969494));
#31707=CARTESIAN_POINT('Ctrl Pts',(0.,7.0366882084607,25.7884785969494));
#31708=CARTESIAN_POINT('Ctrl Pts',(-7.0366882084607,7.0366882084607,25.7884785969494));
#31709=CARTESIAN_POINT('Ctrl Pts',(-7.0366882084607,0.,25.7884785969494));
#31710=CARTESIAN_POINT('Ctrl Pts',(-7.0366882084607,-7.0366882084607,25.7884785969494));
#31711=CARTESIAN_POINT('Ctrl Pts',(0.,-7.0366882084607,25.7884785969494));
#31712=CARTESIAN_POINT('Ctrl Pts',(7.0366882084607,-7.0366882084607,25.7884785969494));
#31713=CARTESIAN_POINT('Ctrl Pts',(7.0366882084607,0.,25.7884785969494));
#31714=CARTESIAN_POINT('Ctrl Pts',(7.65759263692165,0.,25.6543075008141));
#31715=CARTESIAN_POINT('Ctrl Pts',(7.65759263692165,7.65759263692165,25.6543075008141));
#31716=CARTESIAN_POINT('Ctrl Pts',(0.,7.65759263692165,25.6543075008141));
#31717=CARTESIAN_POINT('Ctrl Pts',(-7.65759263692165,7.65759263692165,25.6543075008141));
#31718=CARTESIAN_POINT('Ctrl Pts',(-7.65759263692165,0.,25.6543075008141));
#31719=CARTESIAN_POINT('Ctrl Pts',(-7.65759263692165,-7.65759263692165,
25.6543075008141));
#31720=CARTESIAN_POINT('Ctrl Pts',(0.,-7.65759263692165,25.6543075008141));
#31721=CARTESIAN_POINT('Ctrl Pts',(7.65759263692165,-7.65759263692165,25.6543075008141));
#31722=CARTESIAN_POINT('Ctrl Pts',(7.65759263692165,0.,25.6543075008141));
#31723=CARTESIAN_POINT('Ctrl Pts',(8.27837257578008,0.,25.5159837042088));
#31724=CARTESIAN_POINT('Ctrl Pts',(8.27837257578008,8.27837257578008,25.5159837042088));
#31725=CARTESIAN_POINT('Ctrl Pts',(0.,8.27837257578008,25.5159837042088));
#31726=CARTESIAN_POINT('Ctrl Pts',(-8.27837257578008,8.27837257578008,25.5159837042088));
#31727=CARTESIAN_POINT('Ctrl Pts',(-8.27837257578008,0.,25.5159837042088));
#31728=CARTESIAN_POINT('Ctrl Pts',(-8.27837257578008,-8.27837257578008,
25.5159837042088));
#31729=CARTESIAN_POINT('Ctrl Pts',(0.,-8.27837257578008,25.5159837042088));
#31730=CARTESIAN_POINT('Ctrl Pts',(8.27837257578008,-8.27837257578008,25.5159837042088));
#31731=CARTESIAN_POINT('Ctrl Pts',(8.27837257578008,0.,25.5159837042088));
#31732=CARTESIAN_POINT('Ctrl Pts',(8.89388282563607,0.,25.3769606320571));
#31733=CARTESIAN_POINT('Ctrl Pts',(8.89388282563607,8.89388282563607,25.3769606320571));
#31734=CARTESIAN_POINT('Ctrl Pts',(0.,8.89388282563607,25.3769606320571));
#31735=CARTESIAN_POINT('Ctrl Pts',(-8.89388282563607,8.89388282563607,25.3769606320571));
#31736=CARTESIAN_POINT('Ctrl Pts',(-8.89388282563607,0.,25.3769606320571));
#31737=CARTESIAN_POINT('Ctrl Pts',(-8.89388282563607,-8.89388282563607,
25.3769606320571));
#31738=CARTESIAN_POINT('Ctrl Pts',(0.,-8.89388282563607,25.3769606320571));
#31739=CARTESIAN_POINT('Ctrl Pts',(8.89388282563607,-8.89388282563607,25.3769606320571));
#31740=CARTESIAN_POINT('Ctrl Pts',(8.89388282563607,0.,25.3769606320571));
#31741=CARTESIAN_POINT('Ctrl Pts',(9.49928764562852,0.,25.2405145197409));
#31742=CARTESIAN_POINT('Ctrl Pts',(9.49928764562851,9.49928764562851,25.2405145197409));
#31743=CARTESIAN_POINT('Ctrl Pts',(0.,9.49928764562852,25.2405145197409));
#31744=CARTESIAN_POINT('Ctrl Pts',(-9.49928764562851,9.49928764562851,25.2405145197409));
#31745=CARTESIAN_POINT('Ctrl Pts',(-9.49928764562852,0.,25.2405145197409));
#31746=CARTESIAN_POINT('Ctrl Pts',(-9.49928764562851,-9.49928764562851,
25.2405145197409));
#31747=CARTESIAN_POINT('Ctrl Pts',(0.,-9.49928764562852,25.2405145197409));
#31748=CARTESIAN_POINT('Ctrl Pts',(9.49928764562851,-9.49928764562851,25.2405145197409));
#31749=CARTESIAN_POINT('Ctrl Pts',(9.49928764562852,0.,25.2405145197409));
#31750=CARTESIAN_POINT('Ctrl Pts',(10.0906614723548,0.,25.1093486541428));
#31751=CARTESIAN_POINT('Ctrl Pts',(10.0906614723548,10.0906614723548,25.1093486541428));
#31752=CARTESIAN_POINT('Ctrl Pts',(0.,10.0906614723548,25.1093486541428));
#31753=CARTESIAN_POINT('Ctrl Pts',(-10.0906614723548,10.0906614723548,25.1093486541428));
#31754=CARTESIAN_POINT('Ctrl Pts',(-10.0906614723548,0.,25.1093486541428));
#31755=CARTESIAN_POINT('Ctrl Pts',(-10.0906614723548,-10.0906614723548,
25.1093486541428));
#31756=CARTESIAN_POINT('Ctrl Pts',(0.,-10.0906614723548,25.1093486541428));
#31757=CARTESIAN_POINT('Ctrl Pts',(10.0906614723548,-10.0906614723548,25.1093486541428));
#31758=CARTESIAN_POINT('Ctrl Pts',(10.0906614723548,0.,25.1093486541428));
#31759=CARTESIAN_POINT('Ctrl Pts',(10.6657852303826,0.,24.9850866914374));
#31760=CARTESIAN_POINT('Ctrl Pts',(10.6657852303826,10.6657852303826,24.9850866914374));
#31761=CARTESIAN_POINT('Ctrl Pts',(0.,10.6657852303826,24.9850866914374));
#31762=CARTESIAN_POINT('Ctrl Pts',(-10.6657852303826,10.6657852303826,24.9850866914374));
#31763=CARTESIAN_POINT('Ctrl Pts',(-10.6657852303826,0.,24.9850866914374));
#31764=CARTESIAN_POINT('Ctrl Pts',(-10.6657852303826,-10.6657852303826,
24.9850866914374));
#31765=CARTESIAN_POINT('Ctrl Pts',(0.,-10.6657852303826,24.9850866914374));
#31766=CARTESIAN_POINT('Ctrl Pts',(10.6657852303826,-10.6657852303826,24.9850866914374));
#31767=CARTESIAN_POINT('Ctrl Pts',(10.6657852303826,0.,24.9850866914374));
#31768=CARTESIAN_POINT('Ctrl Pts',(11.2237519652345,0.,24.8684985935572));
#31769=CARTESIAN_POINT('Ctrl Pts',(11.2237519652345,11.2237519652345,24.8684985935572));
#31770=CARTESIAN_POINT('Ctrl Pts',(0.,11.2237519652345,24.8684985935572));
#31771=CARTESIAN_POINT('Ctrl Pts',(-11.2237519652345,11.2237519652345,24.8684985935572));
#31772=CARTESIAN_POINT('Ctrl Pts',(-11.2237519652345,0.,24.8684985935572));
#31773=CARTESIAN_POINT('Ctrl Pts',(-11.2237519652345,-11.2237519652345,
24.8684985935572));
#31774=CARTESIAN_POINT('Ctrl Pts',(0.,-11.2237519652345,24.8684985935572));
#31775=CARTESIAN_POINT('Ctrl Pts',(11.2237519652345,-11.2237519652345,24.8684985935572));
#31776=CARTESIAN_POINT('Ctrl Pts',(11.2237519652345,0.,24.8684985935572));
#31777=CARTESIAN_POINT('Ctrl Pts',(11.6562879503402,0.,24.7815592956469));
#31778=CARTESIAN_POINT('Ctrl Pts',(11.6562879503402,11.6562879503402,24.7815592956469));
#31779=CARTESIAN_POINT('Ctrl Pts',(0.,11.6562879503402,24.7815592956469));
#31780=CARTESIAN_POINT('Ctrl Pts',(-11.6562879503402,11.6562879503402,24.7815592956469));
#31781=CARTESIAN_POINT('Ctrl Pts',(-11.6562879503402,0.,24.7815592956469));
#31782=CARTESIAN_POINT('Ctrl Pts',(-11.6562879503402,-11.6562879503402,
24.7815592956469));
#31783=CARTESIAN_POINT('Ctrl Pts',(0.,-11.6562879503402,24.7815592956469));
#31784=CARTESIAN_POINT('Ctrl Pts',(11.6562879503402,-11.6562879503402,24.7815592956469));
#31785=CARTESIAN_POINT('Ctrl Pts',(11.6562879503402,0.,24.7815592956469));
#31786=CARTESIAN_POINT('Ctrl Pts',(11.97300464761,0.,24.7198967418176));
#31787=CARTESIAN_POINT('Ctrl Pts',(11.97300464761,11.97300464761,24.7198967418176));
#31788=CARTESIAN_POINT('Ctrl Pts',(0.,11.97300464761,24.7198967418176));
#31789=CARTESIAN_POINT('Ctrl Pts',(-11.97300464761,11.97300464761,24.7198967418176));
#31790=CARTESIAN_POINT('Ctrl Pts',(-11.97300464761,0.,24.7198967418176));
#31791=CARTESIAN_POINT('Ctrl Pts',(-11.97300464761,-11.97300464761,24.7198967418176));
#31792=CARTESIAN_POINT('Ctrl Pts',(0.,-11.97300464761,24.7198967418176));
#31793=CARTESIAN_POINT('Ctrl Pts',(11.97300464761,-11.97300464761,24.7198967418176));
#31794=CARTESIAN_POINT('Ctrl Pts',(11.97300464761,0.,24.7198967418176));
#31795=CARTESIAN_POINT('Ctrl Pts',(12.1807579618051,0.,24.6803512815114));
#31796=CARTESIAN_POINT('Ctrl Pts',(12.1807579618051,12.1807579618051,24.6803512815114));
#31797=CARTESIAN_POINT('Ctrl Pts',(0.,12.1807579618051,24.6803512815114));
#31798=CARTESIAN_POINT('Ctrl Pts',(-12.1807579618051,12.1807579618051,24.6803512815114));
#31799=CARTESIAN_POINT('Ctrl Pts',(-12.1807579618051,0.,24.6803512815114));
#31800=CARTESIAN_POINT('Ctrl Pts',(-12.1807579618051,-12.1807579618051,
24.6803512815114));
#31801=CARTESIAN_POINT('Ctrl Pts',(0.,-12.1807579618051,24.6803512815114));
#31802=CARTESIAN_POINT('Ctrl Pts',(12.1807579618051,-12.1807579618051,24.6803512815114));
#31803=CARTESIAN_POINT('Ctrl Pts',(12.1807579618051,0.,24.6803512815114));
#31804=CARTESIAN_POINT('Ctrl Pts',(12.2837868382051,0.,24.6609692735778));
#31805=CARTESIAN_POINT('Ctrl Pts',(12.2837868382051,12.2837868382051,24.6609692735778));
#31806=CARTESIAN_POINT('Ctrl Pts',(0.,12.2837868382051,24.6609692735778));
#31807=CARTESIAN_POINT('Ctrl Pts',(-12.2837868382051,12.2837868382051,24.6609692735778));
#31808=CARTESIAN_POINT('Ctrl Pts',(-12.2837868382051,0.,24.6609692735778));
#31809=CARTESIAN_POINT('Ctrl Pts',(-12.2837868382051,-12.2837868382051,
24.6609692735778));
#31810=CARTESIAN_POINT('Ctrl Pts',(0.,-12.2837868382051,24.6609692735778));
#31811=CARTESIAN_POINT('Ctrl Pts',(12.2837868382051,-12.2837868382051,24.6609692735778));
#31812=CARTESIAN_POINT('Ctrl Pts',(12.2837868382051,0.,24.6609692735778));
#31813=CARTESIAN_POINT('',(2.5,0.,26.4983464639701));
#31814=CARTESIAN_POINT('Ctrl Pts',(2.5,0.,26.4983464639701));
#31815=CARTESIAN_POINT('Ctrl Pts',(2.7,0.,26.4750168877023));
#31816=CARTESIAN_POINT('Ctrl Pts',(2.9,0.,26.4516873114344));
#31817=CARTESIAN_POINT('Ctrl Pts',(3.1,0.,26.4283577351666));
#31818=CARTESIAN_POINT('Ctrl Pts',(3.3,0.,26.4050281588988));
#31819=CARTESIAN_POINT('Ctrl Pts',(3.5,0.,26.381698582631));
#31820=CARTESIAN_POINT('Ctrl Pts',(3.61098900507559,0.,26.368751950337));
#31821=CARTESIAN_POINT('Ctrl Pts',(3.83416205501541,0.,26.3417018678852));
#31822=CARTESIAN_POINT('Ctrl Pts',(4.17250673641263,0.,26.2976563050266));
#31823=CARTESIAN_POINT('Ctrl Pts',(4.63085543889697,0.,26.2319374216757));
#31824=CARTESIAN_POINT('Ctrl Pts',(5.21591518523417,0.,26.137974806988));
#31825=CARTESIAN_POINT('Ctrl Pts',(5.81280340273043,0.,26.0322484636216));
#31826=CARTESIAN_POINT('Ctrl Pts',(6.42047090449388,0.,25.9152983846727));
#31827=CARTESIAN_POINT('Ctrl Pts',(7.0366882084607,0.,25.7884785969494));
#31828=CARTESIAN_POINT('Ctrl Pts',(7.65759263692165,0.,25.6543075008141));
#31829=CARTESIAN_POINT('Ctrl Pts',(8.27837257578008,0.,25.5159837042088));
#31830=CARTESIAN_POINT('Ctrl Pts',(8.89388282563607,0.,25.3769606320571));
#31831=CARTESIAN_POINT('Ctrl Pts',(9.49928764562852,0.,25.2405145197409));
#31832=CARTESIAN_POINT('Ctrl Pts',(10.0906614723548,0.,25.1093486541428));
#31833=CARTESIAN_POINT('Ctrl Pts',(10.6657852303826,0.,24.9850866914374));
#31834=CARTESIAN_POINT('Ctrl Pts',(11.2237519652345,0.,24.8684985935572));
#31835=CARTESIAN_POINT('Ctrl Pts',(11.6562879503402,0.,24.7815592956469));
#31836=CARTESIAN_POINT('Ctrl Pts',(11.97300464761,0.,24.7198967418176));
#31837=CARTESIAN_POINT('Ctrl Pts',(12.1807579618051,0.,24.6803512815114));
#31838=CARTESIAN_POINT('Ctrl Pts',(12.2837868382051,0.,24.6609692735778));
#31839=CARTESIAN_POINT('',(-2.5,-3.06161699786838E-16,26.4983464639701));
#31840=CARTESIAN_POINT('Ctrl Pts',(2.5,-1.47022104461875E-15,26.4983464639701));
#31841=CARTESIAN_POINT('Ctrl Pts',(2.5,-0.0371231848941886,26.4983464639701));
#31842=CARTESIAN_POINT('Ctrl Pts',(2.49917312973535,-0.0742778661173671,
26.4983464639701));
#31843=CARTESIAN_POINT('Ctrl Pts',(2.48367897424576,-0.421532049454881,
26.4983464639701));
#31844=CARTESIAN_POINT('Ctrl Pts',(2.41221020755754,-0.726355581229532,
26.4983464639701));
#31845=CARTESIAN_POINT('Ctrl Pts',(2.15665695254898,-1.30479846977776,26.4983464639701));
#31846=CARTESIAN_POINT('Ctrl Pts',(1.97086325139701,-1.57142174542834,26.4983464639701));
#31847=CARTESIAN_POINT('Ctrl Pts',(1.50189098051651,-2.02580771968822,26.4983464639701));
#31848=CARTESIAN_POINT('Ctrl Pts',(1.22075973154356,-2.20665337385529,26.4983464639701));
#31849=CARTESIAN_POINT('Ctrl Pts',(0.605012462119597,-2.44808145431904,
26.4983464639701));
#31850=CARTESIAN_POINT('Ctrl Pts',(0.276566066778983,-2.50652231129252,
26.4983464639701));
#31851=CARTESIAN_POINT('Ctrl Pts',(-0.363347686367218,-2.49276727488126,
26.4983464639701));
#31852=CARTESIAN_POINT('Ctrl Pts',(-0.669054826467963,-2.42863662722262,
26.4983464639701));
#31853=CARTESIAN_POINT('Ctrl Pts',(-1.25208783868412,-2.18756782255767,
26.4983464639701));
#31854=CARTESIAN_POINT('Ctrl Pts',(-1.52250913573239,-2.00876650352443,
26.4983464639701));
#31855=CARTESIAN_POINT('Ctrl Pts',(-1.99007168793019,-1.54959582229107,
26.4983464639701));
#31856=CARTESIAN_POINT('Ctrl Pts',(-2.17912399473894,-1.27005950691937,
26.4983464639701));
#31857=CARTESIAN_POINT('Ctrl Pts',(-2.4346209083192,-0.656952194285376,
26.4983464639701));
#31858=CARTESIAN_POINT('Ctrl Pts',(-2.5,-0.330098701605058,26.4983464639701));
#31859=CARTESIAN_POINT('Ctrl Pts',(-2.5,-3.7470027081099E-15,26.4983464639701));
#31860=CARTESIAN_POINT('Ctrl Pts',(-2.5,-4.09394740330526E-15,26.4983464639701));
#31861=CARTESIAN_POINT('Ctrl Pts',(-2.5,0.183500133578845,26.4983464639701));
#31862=CARTESIAN_POINT('Ctrl Pts',(-2.47979662058594,0.366443746779873,
26.4983464639701));
#31863=CARTESIAN_POINT('Ctrl Pts',(-2.39698708053327,0.736795527885604,
26.4983464639701));
#31864=CARTESIAN_POINT('Ctrl Pts',(-2.33187346931883,0.922377816972309,
26.4983464639701));
#31865=CARTESIAN_POINT('Ctrl Pts',(-2.10373946785474,1.38879610419602,26.4983464639701));
#31866=CARTESIAN_POINT('Ctrl Pts',(-1.90675062561358,1.64887125615131,26.4983464639701));
#31867=CARTESIAN_POINT('Ctrl Pts',(-1.41891687160025,2.08475912057876,26.4983464639701));
#31868=CARTESIAN_POINT('Ctrl Pts',(-1.13075556057171,2.25409350772863,26.4983464639701));
#31869=CARTESIAN_POINT('Ctrl Pts',(-0.502690476103072,2.47156637397813,
26.4983464639701));
#31870=CARTESIAN_POINT('Ctrl Pts',(-0.168693444061264,2.51652152338796,
26.4983464639701));
#31871=CARTESIAN_POINT('Ctrl Pts',(0.474641333693117,2.47416054609107,26.4983464639701));
#31872=CARTESIAN_POINT('Ctrl Pts',(0.778500559957078,2.395974056961,26.4983464639701));
#31873=CARTESIAN_POINT('Ctrl Pts',(1.3524250977243,2.12722071777005,26.4983464639701));
#31874=CARTESIAN_POINT('Ctrl Pts',(1.61541268207329,1.93508746408567,26.4983464639701));
#31875=CARTESIAN_POINT('Ctrl Pts',(2.05946515295737,1.45539068556724,26.4983464639701));
#31876=CARTESIAN_POINT('Ctrl Pts',(2.2338544798984,1.17023626952827,26.4983464639701));
#31877=CARTESIAN_POINT('Ctrl Pts',(2.44852353908425,0.583828854975951,26.4983464639701));
#31878=CARTESIAN_POINT('Ctrl Pts',(2.5,0.292894735647855,26.4983464639701));
#31879=CARTESIAN_POINT('Ctrl Pts',(2.5,-1.52655665885959E-15,26.4983464639701));
#31880=CARTESIAN_POINT('Origin',(0.,0.,26.1299753788797));
#31881=CARTESIAN_POINT('',(2.49999999999983,-1.916981435175E-33,25.9968387300725));
#31882=CARTESIAN_POINT('',(-2.5,-3.06161699786838E-16,25.9968387300726));
#31883=CARTESIAN_POINT('Ctrl Pts',(2.5,0.,25.9968387300726));
#31884=CARTESIAN_POINT('Ctrl Pts',(2.5,0.0371231848941868,25.9968387300726));
#31885=CARTESIAN_POINT('Ctrl Pts',(2.49917312973534,0.0742778661173646,
25.9968387300726));
#31886=CARTESIAN_POINT('Ctrl Pts',(2.48367897424575,0.421532049454879,25.9968387300726));
#31887=CARTESIAN_POINT('Ctrl Pts',(2.41221020755754,0.726355581229529,25.9968387300726));
#31888=CARTESIAN_POINT('Ctrl Pts',(2.15665695254898,1.30479846977776,25.9968387300726));
#31889=CARTESIAN_POINT('Ctrl Pts',(1.97086325139701,1.57142174542834,25.9968387300726));
#31890=CARTESIAN_POINT('Ctrl Pts',(1.5018909805165,2.02580771968822,25.9968387300726));
#31891=CARTESIAN_POINT('Ctrl Pts',(1.22075973154356,2.20665337385528,25.9968387300726));
#31892=CARTESIAN_POINT('Ctrl Pts',(0.605012462119595,2.44808145431903,25.9968387300726));
#31893=CARTESIAN_POINT('Ctrl Pts',(0.276566066778982,2.50652231129252,25.9968387300726));
#31894=CARTESIAN_POINT('Ctrl Pts',(-0.363347686367218,2.49276727488126,
25.9968387300726));
#31895=CARTESIAN_POINT('Ctrl Pts',(-0.669054826467963,2.42863662722262,
25.9968387300726));
#31896=CARTESIAN_POINT('Ctrl Pts',(-1.25208783868412,2.18756782255767,25.9968387300726));
#31897=CARTESIAN_POINT('Ctrl Pts',(-1.52250913573239,2.00876650352443,25.9968387300726));
#31898=CARTESIAN_POINT('Ctrl Pts',(-1.99007168793019,1.54959582229107,25.9968387300726));
#31899=CARTESIAN_POINT('Ctrl Pts',(-2.17912399473894,1.27005950691936,25.9968387300726));
#31900=CARTESIAN_POINT('Ctrl Pts',(-2.4346209083192,0.656952194285369,25.9968387300726));
#31901=CARTESIAN_POINT('Ctrl Pts',(-2.5,0.330098701605053,25.9968387300726));
#31902=CARTESIAN_POINT('Ctrl Pts',(-2.5,6.93889390390723E-17,25.9968387300726));
#31903=CARTESIAN_POINT('Ctrl Pts',(-2.5,0.,25.9968387300726));
#31904=CARTESIAN_POINT('Ctrl Pts',(-2.5,-0.183500133578844,25.9968387300726));
#31905=CARTESIAN_POINT('Ctrl Pts',(-2.47979662058593,-0.366443746779865,
25.9968387300726));
#31906=CARTESIAN_POINT('Ctrl Pts',(-2.39698708053326,-0.736795527885584,
25.9968387300726));
#31907=CARTESIAN_POINT('Ctrl Pts',(-2.33187346931882,-0.922377816972283,
25.9968387300726));
#31908=CARTESIAN_POINT('Ctrl Pts',(-2.10373946785474,-1.38879610419599,
25.9968387300726));
#31909=CARTESIAN_POINT('Ctrl Pts',(-1.90675062561359,-1.64887125615128,
25.9968387300726));
#31910=CARTESIAN_POINT('Ctrl Pts',(-1.41891687160026,-2.08475912057874,
25.9968387300726));
#31911=CARTESIAN_POINT('Ctrl Pts',(-1.13075556057172,-2.25409350772861,
25.9968387300726));
#31912=CARTESIAN_POINT('Ctrl Pts',(-0.502690476103086,-2.47156637397811,
25.9968387300726));
#31913=CARTESIAN_POINT('Ctrl Pts',(-0.168693444061279,-2.51652152338795,
25.9968387300726));
#31914=CARTESIAN_POINT('Ctrl Pts',(0.474641333693102,-2.47416054609106,
25.9968387300726));
#31915=CARTESIAN_POINT('Ctrl Pts',(0.778500559957062,-2.39597405696099,
25.9968387300726));
#31916=CARTESIAN_POINT('Ctrl Pts',(1.35242509772429,-2.12722071777005,25.9968387300726));
#31917=CARTESIAN_POINT('Ctrl Pts',(1.61541268207328,-1.93508746408567,25.9968387300726));
#31918=CARTESIAN_POINT('Ctrl Pts',(2.05946515295735,-1.45539068556724,25.9968387300726));
#31919=CARTESIAN_POINT('Ctrl Pts',(2.23385447989839,-1.17023626952827,25.9968387300726));
#31920=CARTESIAN_POINT('Ctrl Pts',(2.44852353908424,-0.583828854975953,
25.9968387300726));
#31921=CARTESIAN_POINT('Ctrl Pts',(2.5,-0.292894735647857,25.9968387300726));
#31922=CARTESIAN_POINT('Ctrl Pts',(2.5,0.,25.9968387300726));
#31923=CARTESIAN_POINT('',(-2.5,-3.06161699786838E-16,26.1299753788797));
#31924=CARTESIAN_POINT('Ctrl Pts',(12.0671767507335,0.,24.1930800891729));
#31925=CARTESIAN_POINT('Ctrl Pts',(12.0671767507335,12.0671767507335,24.1930800891729));
#31926=CARTESIAN_POINT('Ctrl Pts',(0.,12.0671767507335,24.1930800891729));
#31927=CARTESIAN_POINT('Ctrl Pts',(-12.0671767507335,12.0671767507335,24.1930800891729));
#31928=CARTESIAN_POINT('Ctrl Pts',(-12.0671767507335,0.,24.1930800891729));
#31929=CARTESIAN_POINT('Ctrl Pts',(-12.0671767507335,-12.0671767507335,
24.1930800891729));
#31930=CARTESIAN_POINT('Ctrl Pts',(0.,-12.0671767507335,24.1930800891729));
#31931=CARTESIAN_POINT('Ctrl Pts',(12.0671767507335,-12.0671767507335,24.1930800891729));
#31932=CARTESIAN_POINT('Ctrl Pts',(12.0671767507335,0.,24.1930800891729));
#31933=CARTESIAN_POINT('Ctrl Pts',(12.0383097771307,0.,24.1985718545699));
#31934=CARTESIAN_POINT('Ctrl Pts',(12.0383097771307,12.0383097771307,24.1985718545699));
#31935=CARTESIAN_POINT('Ctrl Pts',(0.,12.0383097771307,24.1985718545699));
#31936=CARTESIAN_POINT('Ctrl Pts',(-12.0383097771307,12.0383097771307,24.1985718545699));
#31937=CARTESIAN_POINT('Ctrl Pts',(-12.0383097771307,0.,24.1985718545699));
#31938=CARTESIAN_POINT('Ctrl Pts',(-12.0383097771307,-12.0383097771307,
24.1985718545699));
#31939=CARTESIAN_POINT('Ctrl Pts',(0.,-12.0383097771307,24.1985718545699));
#31940=CARTESIAN_POINT('Ctrl Pts',(12.0383097771307,-12.0383097771307,24.1985718545699));
#31941=CARTESIAN_POINT('Ctrl Pts',(12.0383097771307,0.,24.1985718545699));
#31942=CARTESIAN_POINT('Ctrl Pts',(12.0093666549873,0.,24.2040992260835));
#31943=CARTESIAN_POINT('Ctrl Pts',(12.0093666549873,12.0093666549873,24.2040992260835));
#31944=CARTESIAN_POINT('Ctrl Pts',(0.,12.0093666549873,24.2040992260835));
#31945=CARTESIAN_POINT('Ctrl Pts',(-12.0093666549873,12.0093666549873,24.2040992260835));
#31946=CARTESIAN_POINT('Ctrl Pts',(-12.0093666549873,0.,24.2040992260835));
#31947=CARTESIAN_POINT('Ctrl Pts',(-12.0093666549873,-12.0093666549873,
24.2040992260835));
#31948=CARTESIAN_POINT('Ctrl Pts',(0.,-12.0093666549873,24.2040992260835));
#31949=CARTESIAN_POINT('Ctrl Pts',(12.0093666549873,-12.0093666549873,24.2040992260835));
#31950=CARTESIAN_POINT('Ctrl Pts',(12.0093666549873,0.,24.2040992260835));
#31951=CARTESIAN_POINT('Ctrl Pts',(11.9803472472225,0.,24.2096622428817));
#31952=CARTESIAN_POINT('Ctrl Pts',(11.9803472472225,11.9803472472225,24.2096622428817));
#31953=CARTESIAN_POINT('Ctrl Pts',(0.,11.9803472472225,24.2096622428817));
#31954=CARTESIAN_POINT('Ctrl Pts',(-11.9803472472225,11.9803472472225,24.2096622428817));
#31955=CARTESIAN_POINT('Ctrl Pts',(-11.9803472472225,0.,24.2096622428817));
#31956=CARTESIAN_POINT('Ctrl Pts',(-11.9803472472225,-11.9803472472225,
24.2096622428817));
#31957=CARTESIAN_POINT('Ctrl Pts',(0.,-11.9803472472225,24.2096622428817));
#31958=CARTESIAN_POINT('Ctrl Pts',(11.9803472472225,-11.9803472472225,24.2096622428817));
#31959=CARTESIAN_POINT('Ctrl Pts',(11.9803472472225,0.,24.2096622428817));
#31960=CARTESIAN_POINT('Ctrl Pts',(10.7340225064793,0.,24.448582538048));
#31961=CARTESIAN_POINT('Ctrl Pts',(10.7340225064793,10.7340225064793,24.448582538048));
#31962=CARTESIAN_POINT('Ctrl Pts',(0.,10.7340225064793,24.448582538048));
#31963=CARTESIAN_POINT('Ctrl Pts',(-10.7340225064793,10.7340225064793,24.448582538048));
#31964=CARTESIAN_POINT('Ctrl Pts',(-10.7340225064793,0.,24.448582538048));
#31965=CARTESIAN_POINT('Ctrl Pts',(-10.7340225064793,-10.7340225064793,
24.448582538048));
#31966=CARTESIAN_POINT('Ctrl Pts',(0.,-10.7340225064793,24.448582538048));
#31967=CARTESIAN_POINT('Ctrl Pts',(10.7340225064793,-10.7340225064793,24.448582538048));
#31968=CARTESIAN_POINT('Ctrl Pts',(10.7340225064793,0.,24.448582538048));
#31969=CARTESIAN_POINT('Ctrl Pts',(9.31567463360365,0.,24.7734086800262));
#31970=CARTESIAN_POINT('Ctrl Pts',(9.31567463360365,9.31567463360365,24.7734086800262));
#31971=CARTESIAN_POINT('Ctrl Pts',(0.,9.31567463360365,24.7734086800262));
#31972=CARTESIAN_POINT('Ctrl Pts',(-9.31567463360365,9.31567463360365,24.7734086800262));
#31973=CARTESIAN_POINT('Ctrl Pts',(-9.31567463360365,0.,24.7734086800262));
#31974=CARTESIAN_POINT('Ctrl Pts',(-9.31567463360365,-9.31567463360365,
24.7734086800262));
#31975=CARTESIAN_POINT('Ctrl Pts',(0.,-9.31567463360365,24.7734086800262));
#31976=CARTESIAN_POINT('Ctrl Pts',(9.31567463360365,-9.31567463360365,24.7734086800262));
#31977=CARTESIAN_POINT('Ctrl Pts',(9.31567463360365,0.,24.7734086800262));
#31978=CARTESIAN_POINT('Ctrl Pts',(7.85305095226366,0.,25.0981096808978));
#31979=CARTESIAN_POINT('Ctrl Pts',(7.85305095226366,7.85305095226366,25.0981096808978));
#31980=CARTESIAN_POINT('Ctrl Pts',(0.,7.85305095226366,25.0981096808978));
#31981=CARTESIAN_POINT('Ctrl Pts',(-7.85305095226366,7.85305095226366,25.0981096808978));
#31982=CARTESIAN_POINT('Ctrl Pts',(-7.85305095226366,0.,25.0981096808978));
#31983=CARTESIAN_POINT('Ctrl Pts',(-7.85305095226366,-7.85305095226366,
25.0981096808978));
#31984=CARTESIAN_POINT('Ctrl Pts',(0.,-7.85305095226366,25.0981096808978));
#31985=CARTESIAN_POINT('Ctrl Pts',(7.85305095226366,-7.85305095226366,25.0981096808978));
#31986=CARTESIAN_POINT('Ctrl Pts',(7.85305095226366,0.,25.0981096808978));
#31987=CARTESIAN_POINT('Ctrl Pts',(6.33330197010078,0.,25.4354924416704));
#31988=CARTESIAN_POINT('Ctrl Pts',(6.33330197010078,6.33330197010078,25.4354924416704));
#31989=CARTESIAN_POINT('Ctrl Pts',(0.,6.33330197010078,25.4354924416704));
#31990=CARTESIAN_POINT('Ctrl Pts',(-6.33330197010078,6.33330197010078,25.4354924416704));
#31991=CARTESIAN_POINT('Ctrl Pts',(-6.33330197010078,0.,25.4354924416704));
#31992=CARTESIAN_POINT('Ctrl Pts',(-6.33330197010078,-6.33330197010078,
25.4354924416704));
#31993=CARTESIAN_POINT('Ctrl Pts',(0.,-6.33330197010078,25.4354924416704));
#31994=CARTESIAN_POINT('Ctrl Pts',(6.33330197010078,-6.33330197010078,25.4354924416704));
#31995=CARTESIAN_POINT('Ctrl Pts',(6.33330197010078,0.,25.4354924416704));
#31996=CARTESIAN_POINT('Ctrl Pts',(4.84782034806848,0.,25.7184188033672));
#31997=CARTESIAN_POINT('Ctrl Pts',(4.84782034806848,4.84782034806848,25.7184188033672));
#31998=CARTESIAN_POINT('Ctrl Pts',(0.,4.84782034806848,25.7184188033672));
#31999=CARTESIAN_POINT('Ctrl Pts',(-4.84782034806848,4.84782034806848,25.7184188033672));
#32000=CARTESIAN_POINT('Ctrl Pts',(-4.84782034806848,0.,25.7184188033672));
#32001=CARTESIAN_POINT('Ctrl Pts',(-4.84782034806848,-4.84782034806848,
25.7184188033672));
#32002=CARTESIAN_POINT('Ctrl Pts',(0.,-4.84782034806848,25.7184188033672));
#32003=CARTESIAN_POINT('Ctrl Pts',(4.84782034806848,-4.84782034806848,25.7184188033672));
#32004=CARTESIAN_POINT('Ctrl Pts',(4.84782034806848,0.,25.7184188033672));
#32005=CARTESIAN_POINT('Ctrl Pts',(3.50000000000662,0.,25.8782521751276));
#32006=CARTESIAN_POINT('Ctrl Pts',(3.50000000000662,3.50000000000662,25.8782521751276));
#32007=CARTESIAN_POINT('Ctrl Pts',(0.,3.50000000000662,25.8782521751276));
#32008=CARTESIAN_POINT('Ctrl Pts',(-3.50000000000662,3.50000000000662,25.8782521751276));
#32009=CARTESIAN_POINT('Ctrl Pts',(-3.50000000000662,0.,25.8782521751276));
#32010=CARTESIAN_POINT('Ctrl Pts',(-3.50000000000662,-3.50000000000662,
25.8782521751276));
#32011=CARTESIAN_POINT('Ctrl Pts',(0.,-3.50000000000662,25.8782521751276));
#32012=CARTESIAN_POINT('Ctrl Pts',(3.50000000000662,-3.50000000000662,25.8782521751276));
#32013=CARTESIAN_POINT('Ctrl Pts',(3.50000000000662,0.,25.8782521751276));
#32014=CARTESIAN_POINT('Ctrl Pts',(2.66666666667329,0.,25.9770743042478));
#32015=CARTESIAN_POINT('Ctrl Pts',(2.66666666667329,2.66666666667329,25.9770743042478));
#32016=CARTESIAN_POINT('Ctrl Pts',(0.,2.66666666667329,25.9770743042478));
#32017=CARTESIAN_POINT('Ctrl Pts',(-2.66666666667329,2.66666666667329,25.9770743042478));
#32018=CARTESIAN_POINT('Ctrl Pts',(-2.66666666667329,0.,25.9770743042478));
#32019=CARTESIAN_POINT('Ctrl Pts',(-2.66666666667329,-2.66666666667329,
25.9770743042478));
#32020=CARTESIAN_POINT('Ctrl Pts',(0.,-2.66666666667329,25.9770743042478));
#32021=CARTESIAN_POINT('Ctrl Pts',(2.66666666667329,-2.66666666667329,25.9770743042478));
#32022=CARTESIAN_POINT('Ctrl Pts',(2.66666666667329,0.,25.9770743042478));
#32023=CARTESIAN_POINT('Ctrl Pts',(1.83333333333995,0.,26.075896433368));
#32024=CARTESIAN_POINT('Ctrl Pts',(1.83333333333995,1.83333333333995,26.075896433368));
#32025=CARTESIAN_POINT('Ctrl Pts',(0.,1.83333333333995,26.075896433368));
#32026=CARTESIAN_POINT('Ctrl Pts',(-1.83333333333995,1.83333333333995,26.075896433368));
#32027=CARTESIAN_POINT('Ctrl Pts',(-1.83333333333995,0.,26.075896433368));
#32028=CARTESIAN_POINT('Ctrl Pts',(-1.83333333333995,-1.83333333333995,
26.075896433368));
#32029=CARTESIAN_POINT('Ctrl Pts',(0.,-1.83333333333995,26.075896433368));
#32030=CARTESIAN_POINT('Ctrl Pts',(1.83333333333995,-1.83333333333995,26.075896433368));
#32031=CARTESIAN_POINT('Ctrl Pts',(1.83333333333995,0.,26.075896433368));
#32032=CARTESIAN_POINT('Ctrl Pts',(1.00000000000662,0.,26.1747185624882));
#32033=CARTESIAN_POINT('Ctrl Pts',(1.00000000000662,1.00000000000662,26.1747185624882));
#32034=CARTESIAN_POINT('Ctrl Pts',(0.,1.00000000000662,26.1747185624882));
#32035=CARTESIAN_POINT('Ctrl Pts',(-1.00000000000662,1.00000000000662,26.1747185624882));
#32036=CARTESIAN_POINT('Ctrl Pts',(-1.00000000000662,0.,26.1747185624882));
#32037=CARTESIAN_POINT('Ctrl Pts',(-1.00000000000662,-1.00000000000662,
26.1747185624882));
#32038=CARTESIAN_POINT('Ctrl Pts',(0.,-1.00000000000662,26.1747185624882));
#32039=CARTESIAN_POINT('Ctrl Pts',(1.00000000000662,-1.00000000000662,26.1747185624882));
#32040=CARTESIAN_POINT('Ctrl Pts',(1.00000000000662,0.,26.1747185624882));
#32041=CARTESIAN_POINT('',(12.0671767507335,0.,24.193080089173));
#32042=CARTESIAN_POINT('Ctrl Pts',(2.49999999999985,0.,25.9968387300726));
#32043=CARTESIAN_POINT('Ctrl Pts',(2.83333333333544,9.12848302465822E-34,
25.9573098784243));
#32044=CARTESIAN_POINT('Ctrl Pts',(3.16666666667103,-1.27798762345465E-33,
25.917781026776));
#32045=CARTESIAN_POINT('Ctrl Pts',(3.50000000000662,0.,25.8782521751276));
#32046=CARTESIAN_POINT('Ctrl Pts',(4.84782034806848,5.16749317035517E-33,
25.7184188033672));
#32047=CARTESIAN_POINT('Ctrl Pts',(6.33330197010078,-1.15944534749134E-32,
25.4354924416704));
#32048=CARTESIAN_POINT('Ctrl Pts',(7.85305095226366,0.,25.0981096808978));
#32049=CARTESIAN_POINT('Ctrl Pts',(9.31567463360365,5.24203637506798E-32,
24.7734086800262));
#32050=CARTESIAN_POINT('Ctrl Pts',(10.7340225064793,-1.70232317954933E-32,
24.448582538048));
#32051=CARTESIAN_POINT('Ctrl Pts',(11.9803472472225,0.,24.2096622428817));
#32052=CARTESIAN_POINT('Ctrl Pts',(12.0093666549873,1.04782613555734E-31,
24.2040992260835));
#32053=CARTESIAN_POINT('Ctrl Pts',(12.0383097771307,-3.99241436278348E-34,
24.1985718545699));
#32054=CARTESIAN_POINT('Ctrl Pts',(12.0671767507335,0.,24.1930800891729));
#32055=CARTESIAN_POINT('',(-12.0671767507335,-1.47780293825311E-15,24.193080089173));
#32056=CARTESIAN_POINT('Origin',(0.,0.,24.193080089173));
#32057=CARTESIAN_POINT('Origin',(0.,0.,24.193080089173));
#32058=CARTESIAN_POINT('Origin',(0.,0.,25.9634052319394));
#32059=CARTESIAN_POINT('Origin',(-13.4131653526691,-1.64263900155804E-15,
25.9634052319394));
#33463=UNCERTAINTY_MEASURE_WITH_UNIT(LENGTH_MEASURE(0.01),#33475,
'DISTANCE_ACCURACY_VALUE',
'Maximum model space distance between geometric entities at asserted c
onnectivities');
#33467=UNCERTAINTY_MEASURE_WITH_UNIT(LENGTH_MEASURE(0.01),#33475,
'DISTANCE_ACCURACY_VALUE',
'Maximum model space distance between geometric entities at asserted c
onnectivities');
#33470=(
GEOMETRIC_REPRESENTATION_CONTEXT(3)
GLOBAL_UNCERTAINTY_ASSIGNED_CONTEXT((#33463))
GLOBAL_UNIT_ASSIGNED_CONTEXT((#33475,#33477,#33478))
REPRESENTATION_CONTEXT('','3D')
);
#33474=(
GEOMETRIC_REPRESENTATION_CONTEXT(3)
GLOBAL_UNCERTAINTY_ASSIGNED_CONTEXT((#33467))
GLOBAL_UNIT_ASSIGNED_CONTEXT((#33475,#33477,#33478))
REPRESENTATION_CONTEXT('','3D')
);
#33475=(
LENGTH_UNIT()
NAMED_UNIT(*)
SI_UNIT(.MILLI.,.METRE.)
);
#33477=(
NAMED_UNIT(*)
PLANE_ANGLE_UNIT()
SI_UNIT($,.RADIAN.)
);
#33478=(
NAMED_UNIT(*)
SI_UNIT($,.STERADIAN.)
SOLID_ANGLE_UNIT()
);
#33481=SHAPE_DEFINITION_REPRESENTATION(#33487,#33498);
#33487=PRODUCT_DEFINITION_SHAPE('',$,#33505);
#33498=SHAPE_REPRESENTATION('',(#3089),#33470);
#33502=PRODUCT_DEFINITION_CONTEXT('part definition',#33522,'design');
#33505=PRODUCT_DEFINITION('Disc_01','Disc_01',#33511,#33502);
#33511=PRODUCT_DEFINITION_FORMATION('',$,#33526);
#33522=APPLICATION_CONTEXT(
'Core Data for Automotive Mechanical Design Process');
#33523=PRODUCT_CONTEXT('part definition',#33522,'mechanical');
#33526=PRODUCT('Disc_01','Disc_01',$,(#33523));
#33531=PRESENTATION_STYLE_ASSIGNMENT((#33533));
#33533=SURFACE_STYLE_USAGE(.BOTH.,#33535);
#33535=SURFACE_SIDE_STYLE('',(#33537));
#33537=SURFACE_STYLE_FILL_AREA(#33539);
#33539=FILL_AREA_STYLE('Opaque(203,203,203)',(#33541));
#33541=FILL_AREA_STYLE_COLOUR('Opaque(203,203,203)',#33543);
#33543=COLOUR_RGB('Opaque(203,203,203)', 0.09019608, 0.27058824, 0.51372549);
ENDSEC;
END-ISO-10303-21;
